ISO-10303-21;
HEADER;
/* Generated by software containing ST-Developer
 * from STEP Tools, Inc. (www.steptools.com) 
 */

FILE_DESCRIPTION(
/* description */ ('PAT-091'),
/* implementation_level */ '2;1');

FILE_NAME(
/* name */ 'Pivot axle 140 mm (1).step',
/* time_stamp */ '2026-10-27T15:34:44-07:00',
/* author */ (''),
/* organization */ (''),
/* preprocessor_version */ 'ST-DEVELOPER v20.2',
/* originating_system */ 'Autodesk Translation Framework v15.17.0.0',
/* authorisation */ '');

FILE_SCHEMA (('AUTOMOTIVE_DESIGN { 1 0 10303 214 3 1 1 }'));
ENDSEC;

DATA;
#10=MECHANICAL_DESIGN_GEOMETRIC_PRESENTATION_REPRESENTATION('',(#1017),#25100);
#797=SHAPE_REPRESENTATION_RELATIONSHIP('SRR','None',#25561,#907);
#907=ADVANCED_BREP_SHAPE_REPRESENTATION('',(#1139),#25031);
#1017=STYLED_ITEM('',(#26191),#1139);
#1139=MANIFOLD_SOLID_BREP('Body1',#13296);
#1458=FACE_BOUND('',#3511,.T.);
#1459=FACE_BOUND('',#3513,.T.);
#1853=PLANE('',#15354);
#1854=PLANE('',#15358);
#1855=PLANE('',#15362);
#1856=PLANE('',#15363);
#2444=FACE_OUTER_BOUND('',#3505,.T.);
#2445=FACE_OUTER_BOUND('',#3506,.T.);
#2446=FACE_OUTER_BOUND('',#3507,.T.);
#2447=FACE_OUTER_BOUND('',#3508,.T.);
#2448=FACE_OUTER_BOUND('',#3509,.T.);
#2449=FACE_OUTER_BOUND('',#3510,.T.);
#2450=FACE_OUTER_BOUND('',#3512,.T.);
#3505=EDGE_LOOP('',(#10542,#10543,#10544,#10545));
#3506=EDGE_LOOP('',(#10546));
#3507=EDGE_LOOP('',(#10547,#10548,#10549,#10550));
#3508=EDGE_LOOP('',(#10551));
#3509=EDGE_LOOP('',(#10552,#10553,#10554,#10555));
#3510=EDGE_LOOP('',(#10556));
#3511=EDGE_LOOP('',(#10557));
#3512=EDGE_LOOP('',(#10558));
#3513=EDGE_LOOP('',(#10559));
#4572=LINE('',#22769,#5312);
#4573=LINE('',#22776,#5313);
#4574=LINE('',#22783,#5314);
#5312=VECTOR('',#18452,0.164999999999999);
#5313=VECTOR('',#18461,0.164999999999999);
#5314=VECTOR('',#18470,0.600000000000001);
#5937=CIRCLE('',#15352,0.164999999999999);
#5938=CIRCLE('',#15353,0.164999999999999);
#5939=CIRCLE('',#15356,0.164999999999999);
#5940=CIRCLE('',#15357,0.164999999999999);
#5941=CIRCLE('',#15360,0.600000000000001);
#5942=CIRCLE('',#15361,0.600000000000001);
#6904=VERTEX_POINT('',#22766);
#6905=VERTEX_POINT('',#22768);
#6906=VERTEX_POINT('',#22773);
#6907=VERTEX_POINT('',#22775);
#6908=VERTEX_POINT('',#22780);
#6909=VERTEX_POINT('',#22782);
#8206=EDGE_CURVE('',#6904,#6904,#5937,.T.);
#8207=EDGE_CURVE('',#6904,#6905,#4572,.T.);
#8208=EDGE_CURVE('',#6905,#6905,#5938,.T.);
#8209=EDGE_CURVE('',#6906,#6906,#5939,.T.);
#8210=EDGE_CURVE('',#6906,#6907,#4573,.T.);
#8211=EDGE_CURVE('',#6907,#6907,#5940,.T.);
#8212=EDGE_CURVE('',#6908,#6908,#5941,.T.);
#8213=EDGE_CURVE('',#6908,#6909,#4574,.T.);
#8214=EDGE_CURVE('',#6909,#6909,#5942,.T.);
#10542=ORIENTED_EDGE('',*,*,#8206,.F.);
#10543=ORIENTED_EDGE('',*,*,#8207,.T.);
#10544=ORIENTED_EDGE('',*,*,#8208,.F.);
#10545=ORIENTED_EDGE('',*,*,#8207,.F.);
#10546=ORIENTED_EDGE('',*,*,#8206,.T.);
#10547=ORIENTED_EDGE('',*,*,#8209,.F.);
#10548=ORIENTED_EDGE('',*,*,#8210,.T.);
#10549=ORIENTED_EDGE('',*,*,#8211,.T.);
#10550=ORIENTED_EDGE('',*,*,#8210,.F.);
#10551=ORIENTED_EDGE('',*,*,#8211,.F.);
#10552=ORIENTED_EDGE('',*,*,#8212,.F.);
#10553=ORIENTED_EDGE('',*,*,#8213,.T.);
#10554=ORIENTED_EDGE('',*,*,#8214,.T.);
#10555=ORIENTED_EDGE('',*,*,#8213,.F.);
#10556=ORIENTED_EDGE('',*,*,#8212,.T.);
#10557=ORIENTED_EDGE('',*,*,#8208,.T.);
#10558=ORIENTED_EDGE('',*,*,#8214,.F.);
#10559=ORIENTED_EDGE('',*,*,#8209,.T.);
#12235=CYLINDRICAL_SURFACE('',#15351,0.164999999999999);
#12236=CYLINDRICAL_SURFACE('',#15355,0.164999999999999);
#12237=CYLINDRICAL_SURFACE('',#15359,0.600000000000001);
#12811=ADVANCED_FACE('',(#2444),#12235,.F.);
#12812=ADVANCED_FACE('',(#2445),#1853,.T.);
#12813=ADVANCED_FACE('',(#2446),#12236,.F.);
#12814=ADVANCED_FACE('',(#2447),#1854,.F.);
#12815=ADVANCED_FACE('',(#2448),#12237,.T.);
#12816=ADVANCED_FACE('',(#2449,#1458),#1855,.T.);
#12817=ADVANCED_FACE('',(#2450,#1459),#1856,.F.);
#13296=CLOSED_SHELL('',(#12811,#12812,#12813,#12814,#12815,#12816,#12817));
#15350=AXIS2_PLACEMENT_3D('',#22764,#18446,#18447);
#15351=AXIS2_PLACEMENT_3D('',#22765,#18448,#18449);
#15352=AXIS2_PLACEMENT_3D('',#22767,#18450,#18451);
#15353=AXIS2_PLACEMENT_3D('',#22770,#18453,#18454);
#15354=AXIS2_PLACEMENT_3D('',#22771,#18455,#18456);
#15355=AXIS2_PLACEMENT_3D('',#22772,#18457,#18458);
#15356=AXIS2_PLACEMENT_3D('',#22774,#18459,#18460);
#15357=AXIS2_PLACEMENT_3D('',#22777,#18462,#18463);
#15358=AXIS2_PLACEMENT_3D('',#22778,#18464,#18465);
#15359=AXIS2_PLACEMENT_3D('',#22779,#18466,#18467);
#15360=AXIS2_PLACEMENT_3D('',#22781,#18468,#18469);
#15361=AXIS2_PLACEMENT_3D('',#22784,#18471,#18472);
#15362=AXIS2_PLACEMENT_3D('',#22785,#18473,#18474);
#15363=AXIS2_PLACEMENT_3D('',#22786,#18475,#18476);
#18446=DIRECTION('axis',(0.,0.,1.));
#18447=DIRECTION('refdir',(1.,0.,0.));
#18448=DIRECTION('center_axis',(0.,1.,0.));
#18449=DIRECTION('ref_axis',(1.,0.,0.));
#18450=DIRECTION('center_axis',(0.,1.,0.));
#18451=DIRECTION('ref_axis',(1.,0.,0.));
#18452=DIRECTION('',(0.,1.,0.));
#18453=DIRECTION('center_axis',(0.,-1.,0.));
#18454=DIRECTION('ref_axis',(1.,0.,0.));
#18455=DIRECTION('center_axis',(0.,1.,0.));
#18456=DIRECTION('ref_axis',(1.,0.,0.));
#18457=DIRECTION('center_axis',(0.,1.,0.));
#18458=DIRECTION('ref_axis',(1.,0.,0.));
#18459=DIRECTION('center_axis',(0.,1.,0.));
#18460=DIRECTION('ref_axis',(1.,0.,0.));
#18461=DIRECTION('',(0.,1.,0.));
#18462=DIRECTION('center_axis',(0.,1.,0.));
#18463=DIRECTION('ref_axis',(1.,0.,0.));
#18464=DIRECTION('center_axis',(0.,1.,0.));
#18465=DIRECTION('ref_axis',(1.,0.,0.));
#18466=DIRECTION('center_axis',(0.,1.,0.));
#18467=DIRECTION('ref_axis',(1.,0.,0.));
#18468=DIRECTION('center_axis',(0.,1.,0.));
#18469=DIRECTION('ref_axis',(1.,0.,0.));
#18470=DIRECTION('',(0.,-1.,0.));
#18471=DIRECTION('center_axis',(0.,1.,0.));
#18472=DIRECTION('ref_axis',(1.,0.,0.));
#18473=DIRECTION('center_axis',(0.,1.,0.));
#18474=DIRECTION('ref_axis',(1.,0.,0.));
#18475=DIRECTION('center_axis',(0.,1.,0.));
#18476=DIRECTION('ref_axis',(1.,0.,0.));
#22764=CARTESIAN_POINT('',(0.,0.,0.));
#22765=CARTESIAN_POINT('Origin',(38.7298334620742,4.9,13.));
#22766=CARTESIAN_POINT('',(38.5648334620742,4.9,13.));
#22767=CARTESIAN_POINT('Origin',(38.7298334620742,4.9,13.));
#22768=CARTESIAN_POINT('',(38.5648334620742,6.5,13.));
#22769=CARTESIAN_POINT('',(38.5648334620742,4.9,13.));
#22770=CARTESIAN_POINT('Origin',(38.7298334620742,6.5,13.));
#22771=CARTESIAN_POINT('Origin',(38.7298334620742,4.9,13.));
#22772=CARTESIAN_POINT('Origin',(38.7298334620742,-7.6,13.));
#22773=CARTESIAN_POINT('',(38.5648334620742,-7.5,13.));
#22774=CARTESIAN_POINT('Origin',(38.7298334620742,-7.5,13.));
#22775=CARTESIAN_POINT('',(38.5648334620742,-5.9,13.));
#22776=CARTESIAN_POINT('',(38.5648334620742,-7.6,13.));
#22777=CARTESIAN_POINT('Origin',(38.7298334620742,-5.9,13.));
#22778=CARTESIAN_POINT('Origin',(38.7298334620742,-5.9,13.));
#22779=CARTESIAN_POINT('Origin',(38.7298334620742,-7.5,13.));
#22780=CARTESIAN_POINT('',(38.1298334620742,6.5,13.));
#22781=CARTESIAN_POINT('Origin',(38.7298334620742,6.5,13.));
#22782=CARTESIAN_POINT('',(38.1298334620742,-7.5,13.));
#22783=CARTESIAN_POINT('',(38.1298334620742,-7.5,13.));
#22784=CARTESIAN_POINT('Origin',(38.7298334620742,-7.5,13.));
#22785=CARTESIAN_POINT('Origin',(38.7298334620742,6.5,13.));
#22786=CARTESIAN_POINT('Origin',(38.7298334620742,-7.5,13.));
#24910=UNCERTAINTY_MEASURE_WITH_UNIT(LENGTH_MEASURE(0.001),#25101,
'DISTANCE_ACCURACY_VALUE',
'Maximum model space distance between geometric entities at asserted c
onnectivities');
#24979=UNCERTAINTY_MEASURE_WITH_UNIT(LENGTH_MEASURE(0.001),#25101,
'DISTANCE_ACCURACY_VALUE',
'Maximum model space distance between geometric entities at asserted c
onnectivities');
#25031=(
GEOMETRIC_REPRESENTATION_CONTEXT(3)
GLOBAL_UNCERTAINTY_ASSIGNED_CONTEXT((#24910))
GLOBAL_UNIT_ASSIGNED_CONTEXT((#25101,#25103,#25104))
REPRESENTATION_CONTEXT('','3D')
);
#25100=(
GEOMETRIC_REPRESENTATION_CONTEXT(3)
GLOBAL_UNCERTAINTY_ASSIGNED_CONTEXT((#24979))
GLOBAL_UNIT_ASSIGNED_CONTEXT((#25101,#25103,#25104))
REPRESENTATION_CONTEXT('','3D')
);
#25101=(
LENGTH_UNIT()
NAMED_UNIT(*)
SI_UNIT(.CENTI.,.METRE.)
);
#25103=(
NAMED_UNIT(*)
PLANE_ANGLE_UNIT()
SI_UNIT($,.RADIAN.)
);
#25104=(
NAMED_UNIT(*)
SI_UNIT($,.STERADIAN.)
SOLID_ANGLE_UNIT()
);
#25156=SHAPE_DEFINITION_REPRESENTATION(#25276,#25561);
#25276=PRODUCT_DEFINITION_SHAPE('',$,#25682);
#25561=SHAPE_REPRESENTATION('',(#15350),#25031);
#25630=PRODUCT_DEFINITION_CONTEXT('part definition',#25992,'design');
#25682=PRODUCT_DEFINITION('Pivot axle 140 mm (1)','Pivot axle 140 mm (1)',
#25802,#25630);
#25802=PRODUCT_DEFINITION_FORMATION('',$,#26045);
#25992=APPLICATION_CONTEXT(
'Core Data for Automotive Mechanical Design Process');
#25993=PRODUCT_CONTEXT('part definition',#25992,'mechanical');
#26045=PRODUCT('Pivot axle 140 mm (1)','Pivot axle 140 mm (1)',
'Pivot axle 140 mm (1)',(#25993));
#26185=COLOUR_RGB('Grey',0.48,0.52,0.57);
#26186=FILL_AREA_STYLE_COLOUR('',#26185);
#26187=FILL_AREA_STYLE('',(#26186));
#26188=SURFACE_STYLE_FILL_AREA(#26187);
#26189=SURFACE_SIDE_STYLE('',(#26188));
#26190=SURFACE_STYLE_USAGE(.BOTH.,#26189);
#26191=PRESENTATION_STYLE_ASSIGNMENT((#26190));
ENDSEC;
END-ISO-10303-21;
